ISO-10303-21;
HEADER;
/* Generated by software containing ST-Developer
 * from STEP Tools, Inc. (www.steptools.com) 
 */

FILE_DESCRIPTION(
/* description */ ('Dual-rail gantry carriage'),
/* implementation_level */ '2;1');

FILE_NAME(
/* name */ 'M5x14 Cap Screw.step',
/* time_stamp */ '2026-10-27T10:49:15-07:00',
/* author */ (''),
/* organization */ (''),
/* preprocessor_version */ 'ST-DEVELOPER v20.2',
/* originating_system */ 'Autodesk Translation Framework v15.17.0.0',
/* authorisation */ '');

FILE_SCHEMA (('AUTOMOTIVE_DESIGN { 1 0 10303 214 3 1 1 }'));
ENDSEC;

DATA;
#10=MECHANICAL_DESIGN_GEOMETRIC_PRESENTATION_REPRESENTATION('',(#603),#12804);
#494=ORIENTED_CLOSED_SHELL('',*,#7382,.F.);
#502=CONICAL_SURFACE('',#8098,0.4,0.785398163397448);
#503=CONICAL_SURFACE('',#8102,0.41,0.785398163397448);
#504=CONICAL_SURFACE('',#8106,0.26,0.463647609000806);
#519=BREP_WITH_VOIDS('Body1',#7383,(#494));
#541=SHAPE_REPRESENTATION_RELATIONSHIP('SRR','None',#13019,#572);
#572=ADVANCED_BREP_SHAPE_REPRESENTATION('',(#519),#12789);
#603=STYLED_ITEM('',(#13254),#519);
#706=FACE_BOUND('',#1743,.T.);
#944=PLANE('',#8086);
#945=PLANE('',#8087);
#946=PLANE('',#8088);
#947=PLANE('',#8089);
#948=PLANE('',#8090);
#949=PLANE('',#8091);
#950=PLANE('',#8092);
#951=PLANE('',#8093);
#952=PLANE('',#8094);
#953=PLANE('',#8096);
#954=PLANE('',#8104);
#1276=FACE_OUTER_BOUND('',#1729,.T.);
#1277=FACE_OUTER_BOUND('',#1730,.T.);
#1278=FACE_OUTER_BOUND('',#1731,.T.);
#1279=FACE_OUTER_BOUND('',#1732,.T.);
#1280=FACE_OUTER_BOUND('',#1733,.T.);
#1281=FACE_OUTER_BOUND('',#1734,.T.);
#1282=FACE_OUTER_BOUND('',#1735,.T.);
#1283=FACE_OUTER_BOUND('',#1736,.T.);
#1284=FACE_OUTER_BOUND('',#1737,.T.);
#1285=FACE_OUTER_BOUND('',#1738,.T.);
#1286=FACE_OUTER_BOUND('',#1739,.T.);
#1287=FACE_OUTER_BOUND('',#1740,.T.);
#1288=FACE_OUTER_BOUND('',#1741,.T.);
#1289=FACE_OUTER_BOUND('',#1742,.T.);
#1290=FACE_OUTER_BOUND('',#1744,.T.);
#1291=FACE_OUTER_BOUND('',#1745,.T.);
#1729=EDGE_LOOP('',(#6159,#6160,#6161,#6162));
#1730=EDGE_LOOP('',(#6163,#6164,#6165,#6166));
#1731=EDGE_LOOP('',(#6167,#6168,#6169,#6170));
#1732=EDGE_LOOP('',(#6171,#6172,#6173,#6174));
#1733=EDGE_LOOP('',(#6175,#6176,#6177,#6178));
#1734=EDGE_LOOP('',(#6179,#6180,#6181,#6182));
#1735=EDGE_LOOP('',(#6183,#6184,#6185,#6186,#6187,#6188));
#1736=EDGE_LOOP('',(#6189,#6190,#6191,#6192,#6193,#6194));
#1737=EDGE_LOOP('',(#6195));
#1738=EDGE_LOOP('',(#6196));
#1739=EDGE_LOOP('',(#6197,#6198,#6199,#6200));
#1740=EDGE_LOOP('',(#6201,#6202,#6203,#6204));
#1741=EDGE_LOOP('',(#6205,#6206,#6207,#6208));
#1742=EDGE_LOOP('',(#6209));
#1743=EDGE_LOOP('',(#6210));
#1744=EDGE_LOOP('',(#6211,#6212,#6213,#6214));
#1745=EDGE_LOOP('',(#6215,#6216,#6217,#6218));
#2398=LINE('',#11838,#3107);
#2399=LINE('',#11840,#3108);
#2400=LINE('',#11842,#3109);
#2401=LINE('',#11843,#3110);
#2402=LINE('',#11846,#3111);
#2403=LINE('',#11848,#3112);
#2404=LINE('',#11849,#3113);
#2405=LINE('',#11852,#3114);
#2406=LINE('',#11854,#3115);
#2407=LINE('',#11855,#3116);
#2408=LINE('',#11858,#3117);
#2409=LINE('',#11860,#3118);
#2410=LINE('',#11861,#3119);
#2411=LINE('',#11864,#3120);
#2412=LINE('',#11866,#3121);
#2413=LINE('',#11867,#3122);
#2414=LINE('',#11869,#3123);
#2415=LINE('',#11870,#3124);
#2416=LINE('',#11882,#3125);
#2417=LINE('',#11886,#3126);
#2418=LINE('',#11890,#3127);
#2419=LINE('',#11897,#3128);
#2420=LINE('',#11899,#3129);
#3107=VECTOR('',#9629,1.);
#3108=VECTOR('',#9630,1.);
#3109=VECTOR('',#9631,1.);
#3110=VECTOR('',#9632,1.);
#3111=VECTOR('',#9635,1.);
#3112=VECTOR('',#9636,1.);
#3113=VECTOR('',#9637,1.);
#3114=VECTOR('',#9640,1.);
#3115=VECTOR('',#9641,1.);
#3116=VECTOR('',#9642,1.);
#3117=VECTOR('',#9645,1.);
#3118=VECTOR('',#9646,1.);
#3119=VECTOR('',#9647,1.);
#3120=VECTOR('',#9650,1.);
#3121=VECTOR('',#9651,1.);
#3122=VECTOR('',#9652,1.);
#3123=VECTOR('',#9655,1.);
#3124=VECTOR('',#9656,1.);
#3125=VECTOR('',#9673,0.4);
#3126=VECTOR('',#9678,0.425);
#3127=VECTOR('',#9683,0.41);
#3128=VECTOR('',#9692,0.26);
#3129=VECTOR('',#9695,0.25);
#3460=CIRCLE('',#8095,0.24505);
#3461=CIRCLE('',#8097,0.375);
#3462=CIRCLE('',#8099,0.425);
#3463=CIRCLE('',#8101,0.425);
#3464=CIRCLE('',#8103,0.395);
#3465=CIRCLE('',#8105,0.27);
#3466=CIRCLE('',#8107,0.24505);
#3918=VERTEX_POINT('',#11836);
#3919=VERTEX_POINT('',#11837);
#3920=VERTEX_POINT('',#11839);
#3921=VERTEX_POINT('',#11841);
#3922=VERTEX_POINT('',#11845);
#3923=VERTEX_POINT('',#11847);
#3924=VERTEX_POINT('',#11851);
#3925=VERTEX_POINT('',#11853);
#3926=VERTEX_POINT('',#11857);
#3927=VERTEX_POINT('',#11859);
#3928=VERTEX_POINT('',#11863);
#3929=VERTEX_POINT('',#11865);
#3930=VERTEX_POINT('',#11874);
#3931=VERTEX_POINT('',#11877);
#3932=VERTEX_POINT('',#11880);
#3933=VERTEX_POINT('',#11884);
#3934=VERTEX_POINT('',#11888);
#3935=VERTEX_POINT('',#11892);
#3936=VERTEX_POINT('',#11895);
#4702=EDGE_CURVE('',#3918,#3919,#2398,.T.);
#4703=EDGE_CURVE('',#3919,#3920,#2399,.T.);
#4704=EDGE_CURVE('',#3920,#3921,#2400,.T.);
#4705=EDGE_CURVE('',#3918,#3921,#2401,.T.);
#4706=EDGE_CURVE('',#3919,#3922,#2402,.T.);
#4707=EDGE_CURVE('',#3922,#3923,#2403,.T.);
#4708=EDGE_CURVE('',#3923,#3920,#2404,.T.);
#4709=EDGE_CURVE('',#3922,#3924,#2405,.T.);
#4710=EDGE_CURVE('',#3924,#3925,#2406,.T.);
#4711=EDGE_CURVE('',#3925,#3923,#2407,.T.);
#4712=EDGE_CURVE('',#3924,#3926,#2408,.T.);
#4713=EDGE_CURVE('',#3926,#3927,#2409,.T.);
#4714=EDGE_CURVE('',#3927,#3925,#2410,.T.);
#4715=EDGE_CURVE('',#3926,#3928,#2411,.T.);
#4716=EDGE_CURVE('',#3928,#3929,#2412,.T.);
#4717=EDGE_CURVE('',#3929,#3927,#2413,.T.);
#4718=EDGE_CURVE('',#3928,#3918,#2414,.T.);
#4719=EDGE_CURVE('',#3921,#3929,#2415,.T.);
#4720=EDGE_CURVE('',#3930,#3930,#3460,.T.);
#4721=EDGE_CURVE('',#3931,#3931,#3461,.T.);
#4722=EDGE_CURVE('',#3932,#3932,#3462,.T.);
#4723=EDGE_CURVE('',#3932,#3931,#2416,.T.);
#4724=EDGE_CURVE('',#3933,#3933,#3463,.T.);
#4725=EDGE_CURVE('',#3933,#3932,#2417,.T.);
#4726=EDGE_CURVE('',#3934,#3934,#3464,.T.);
#4727=EDGE_CURVE('',#3934,#3933,#2418,.T.);
#4728=EDGE_CURVE('',#3935,#3935,#3465,.T.);
#4729=EDGE_CURVE('',#3936,#3936,#3466,.F.);
#4730=EDGE_CURVE('',#3936,#3935,#2419,.T.);
#4731=EDGE_CURVE('',#3930,#3936,#2420,.T.);
#6159=ORIENTED_EDGE('',*,*,#4702,.T.);
#6160=ORIENTED_EDGE('',*,*,#4703,.T.);
#6161=ORIENTED_EDGE('',*,*,#4704,.T.);
#6162=ORIENTED_EDGE('',*,*,#4705,.F.);
#6163=ORIENTED_EDGE('',*,*,#4706,.T.);
#6164=ORIENTED_EDGE('',*,*,#4707,.T.);
#6165=ORIENTED_EDGE('',*,*,#4708,.T.);
#6166=ORIENTED_EDGE('',*,*,#4703,.F.);
#6167=ORIENTED_EDGE('',*,*,#4709,.T.);
#6168=ORIENTED_EDGE('',*,*,#4710,.T.);
#6169=ORIENTED_EDGE('',*,*,#4711,.T.);
#6170=ORIENTED_EDGE('',*,*,#4707,.F.);
#6171=ORIENTED_EDGE('',*,*,#4712,.T.);
#6172=ORIENTED_EDGE('',*,*,#4713,.T.);
#6173=ORIENTED_EDGE('',*,*,#4714,.T.);
#6174=ORIENTED_EDGE('',*,*,#4710,.F.);
#6175=ORIENTED_EDGE('',*,*,#4715,.T.);
#6176=ORIENTED_EDGE('',*,*,#4716,.T.);
#6177=ORIENTED_EDGE('',*,*,#4717,.T.);
#6178=ORIENTED_EDGE('',*,*,#4713,.F.);
#6179=ORIENTED_EDGE('',*,*,#4718,.T.);
#6180=ORIENTED_EDGE('',*,*,#4705,.T.);
#6181=ORIENTED_EDGE('',*,*,#4719,.T.);
#6182=ORIENTED_EDGE('',*,*,#4716,.F.);
#6183=ORIENTED_EDGE('',*,*,#4718,.F.);
#6184=ORIENTED_EDGE('',*,*,#4715,.F.);
#6185=ORIENTED_EDGE('',*,*,#4712,.F.);
#6186=ORIENTED_EDGE('',*,*,#4709,.F.);
#6187=ORIENTED_EDGE('',*,*,#4706,.F.);
#6188=ORIENTED_EDGE('',*,*,#4702,.F.);
#6189=ORIENTED_EDGE('',*,*,#4719,.F.);
#6190=ORIENTED_EDGE('',*,*,#4704,.F.);
#6191=ORIENTED_EDGE('',*,*,#4708,.F.);
#6192=ORIENTED_EDGE('',*,*,#4711,.F.);
#6193=ORIENTED_EDGE('',*,*,#4714,.F.);
#6194=ORIENTED_EDGE('',*,*,#4717,.F.);
#6195=ORIENTED_EDGE('',*,*,#4720,.F.);
#6196=ORIENTED_EDGE('',*,*,#4721,.F.);
#6197=ORIENTED_EDGE('',*,*,#4722,.F.);
#6198=ORIENTED_EDGE('',*,*,#4723,.T.);
#6199=ORIENTED_EDGE('',*,*,#4721,.T.);
#6200=ORIENTED_EDGE('',*,*,#4723,.F.);
#6201=ORIENTED_EDGE('',*,*,#4724,.F.);
#6202=ORIENTED_EDGE('',*,*,#4725,.T.);
#6203=ORIENTED_EDGE('',*,*,#4722,.T.);
#6204=ORIENTED_EDGE('',*,*,#4725,.F.);
#6205=ORIENTED_EDGE('',*,*,#4726,.F.);
#6206=ORIENTED_EDGE('',*,*,#4727,.T.);
#6207=ORIENTED_EDGE('',*,*,#4724,.T.);
#6208=ORIENTED_EDGE('',*,*,#4727,.F.);
#6209=ORIENTED_EDGE('',*,*,#4726,.T.);
#6210=ORIENTED_EDGE('',*,*,#4728,.F.);
#6211=ORIENTED_EDGE('',*,*,#4729,.F.);
#6212=ORIENTED_EDGE('',*,*,#4730,.T.);
#6213=ORIENTED_EDGE('',*,*,#4728,.T.);
#6214=ORIENTED_EDGE('',*,*,#4730,.F.);
#6215=ORIENTED_EDGE('',*,*,#4720,.T.);
#6216=ORIENTED_EDGE('',*,*,#4731,.T.);
#6217=ORIENTED_EDGE('',*,*,#4729,.T.);
#6218=ORIENTED_EDGE('',*,*,#4731,.F.);
#6933=CYLINDRICAL_SURFACE('',#8100,0.425);
#6934=CYLINDRICAL_SURFACE('',#8108,0.24505);
#7202=ADVANCED_FACE('',(#1276),#944,.F.);
#7203=ADVANCED_FACE('',(#1277),#945,.F.);
#7204=ADVANCED_FACE('',(#1278),#946,.F.);
#7205=ADVANCED_FACE('',(#1279),#947,.F.);
#7206=ADVANCED_FACE('',(#1280),#948,.F.);
#7207=ADVANCED_FACE('',(#1281),#949,.F.);
#7208=ADVANCED_FACE('',(#1282),#950,.F.);
#7209=ADVANCED_FACE('',(#1283),#951,.F.);
#7210=ADVANCED_FACE('',(#1284),#952,.F.);
#7211=ADVANCED_FACE('',(#1285),#953,.T.);
#7212=ADVANCED_FACE('',(#1286),#502,.T.);
#7213=ADVANCED_FACE('',(#1287),#6933,.T.);
#7214=ADVANCED_FACE('',(#1288),#503,.T.);
#7215=ADVANCED_FACE('',(#1289,#706),#954,.T.);
#7216=ADVANCED_FACE('',(#1290),#504,.T.);
#7217=ADVANCED_FACE('',(#1291),#6934,.T.);
#7382=CLOSED_SHELL('',(#7202,#7203,#7204,#7205,#7206,#7207,#7208,#7209));
#7383=CLOSED_SHELL('',(#7210,#7211,#7212,#7213,#7214,#7215,#7216,#7217));
#8085=AXIS2_PLACEMENT_3D('',#11834,#9625,#9626);
#8086=AXIS2_PLACEMENT_3D('',#11835,#9627,#9628);
#8087=AXIS2_PLACEMENT_3D('',#11844,#9633,#9634);
#8088=AXIS2_PLACEMENT_3D('',#11850,#9638,#9639);
#8089=AXIS2_PLACEMENT_3D('',#11856,#9643,#9644);
#8090=AXIS2_PLACEMENT_3D('',#11862,#9648,#9649);
#8091=AXIS2_PLACEMENT_3D('',#11868,#9653,#9654);
#8092=AXIS2_PLACEMENT_3D('',#11871,#9657,#9658);
#8093=AXIS2_PLACEMENT_3D('',#11872,#9659,#9660);
#8094=AXIS2_PLACEMENT_3D('',#11873,#9661,#9662);
#8095=AXIS2_PLACEMENT_3D('',#11875,#9663,#9664);
#8096=AXIS2_PLACEMENT_3D('',#11876,#9665,#9666);
#8097=AXIS2_PLACEMENT_3D('',#11878,#9667,#9668);
#8098=AXIS2_PLACEMENT_3D('',#11879,#9669,#9670);
#8099=AXIS2_PLACEMENT_3D('',#11881,#9671,#9672);
#8100=AXIS2_PLACEMENT_3D('',#11883,#9674,#9675);
#8101=AXIS2_PLACEMENT_3D('',#11885,#9676,#9677);
#8102=AXIS2_PLACEMENT_3D('',#11887,#9679,#9680);
#8103=AXIS2_PLACEMENT_3D('',#11889,#9681,#9682);
#8104=AXIS2_PLACEMENT_3D('',#11891,#9684,#9685);
#8105=AXIS2_PLACEMENT_3D('',#11893,#9686,#9687);
#8106=AXIS2_PLACEMENT_3D('',#11894,#9688,#9689);
#8107=AXIS2_PLACEMENT_3D('',#11896,#9690,#9691);
#8108=AXIS2_PLACEMENT_3D('',#11898,#9693,#9694);
#9625=DIRECTION('axis',(0.,0.,1.));
#9626=DIRECTION('refdir',(1.,0.,0.));
#9627=DIRECTION('center_axis',(0.866025403784439,0.,-0.5));
#9628=DIRECTION('ref_axis',(0.5,0.,0.866025403784439));
#9629=DIRECTION('',(-0.5,0.,-0.866025403784439));
#9630=DIRECTION('',(0.,-1.,0.));
#9631=DIRECTION('',(0.5,0.,0.866025403784439));
#9632=DIRECTION('',(0.,-1.,0.));
#9633=DIRECTION('center_axis',(1.20185167898973E-16,0.,-1.));
#9634=DIRECTION('ref_axis',(1.,0.,1.20185167898973E-16));
#9635=DIRECTION('',(-1.,0.,-1.20185167898973E-16));
#9636=DIRECTION('',(0.,-1.,0.));
#9637=DIRECTION('',(1.,0.,1.20185167898973E-16));
#9638=DIRECTION('center_axis',(-0.866025403784439,0.,-0.5));
#9639=DIRECTION('ref_axis',(0.5,0.,-0.866025403784439));
#9640=DIRECTION('',(-0.5,0.,0.866025403784439));
#9641=DIRECTION('',(0.,-1.,0.));
#9642=DIRECTION('',(0.5,0.,-0.866025403784439));
#9643=DIRECTION('center_axis',(-0.866025403784439,0.,0.5));
#9644=DIRECTION('ref_axis',(-0.5,0.,-0.866025403784439));
#9645=DIRECTION('',(0.5,0.,0.866025403784439));
#9646=DIRECTION('',(0.,-1.,0.));
#9647=DIRECTION('',(-0.5,0.,-0.866025403784439));
#9648=DIRECTION('center_axis',(-2.40370335797945E-16,0.,1.));
#9649=DIRECTION('ref_axis',(-1.,0.,-2.40370335797945E-16));
#9650=DIRECTION('',(1.,0.,2.40370335797945E-16));
#9651=DIRECTION('',(0.,-1.,0.));
#9652=DIRECTION('',(-1.,0.,-2.40370335797945E-16));
#9653=DIRECTION('center_axis',(0.866025403784439,0.,0.5));
#9654=DIRECTION('ref_axis',(-0.5,0.,0.866025403784439));
#9655=DIRECTION('',(0.5,0.,-0.866025403784439));
#9656=DIRECTION('',(-0.5,0.,0.866025403784439));
#9657=DIRECTION('center_axis',(0.,1.,0.));
#9658=DIRECTION('ref_axis',(1.,0.,0.));
#9659=DIRECTION('center_axis',(0.,-1.,0.));
#9660=DIRECTION('ref_axis',(0.,0.,-1.));
#9661=DIRECTION('center_axis',(0.,1.,0.));
#9662=DIRECTION('ref_axis',(1.,0.,0.));
#9663=DIRECTION('center_axis',(0.,1.,0.));
#9664=DIRECTION('ref_axis',(1.,0.,0.));
#9665=DIRECTION('center_axis',(0.,1.,0.));
#9666=DIRECTION('ref_axis',(0.,0.,1.));
#9667=DIRECTION('center_axis',(0.,-1.,0.));
#9668=DIRECTION('ref_axis',(1.,0.,0.));
#9669=DIRECTION('center_axis',(0.,-1.,0.));
#9670=DIRECTION('ref_axis',(1.,0.,0.));
#9671=DIRECTION('center_axis',(0.,-1.,0.));
#9672=DIRECTION('ref_axis',(1.,0.,0.));
#9673=DIRECTION('',(0.707106781186548,0.707106781186547,8.65956056235493E-17));
#9674=DIRECTION('center_axis',(0.,-1.,0.));
#9675=DIRECTION('ref_axis',(1.,0.,0.));
#9676=DIRECTION('center_axis',(0.,-1.,0.));
#9677=DIRECTION('ref_axis',(1.,0.,0.));
#9678=DIRECTION('',(0.,1.,0.));
#9679=DIRECTION('center_axis',(0.,1.,0.));
#9680=DIRECTION('ref_axis',(1.,0.,0.));
#9681=DIRECTION('center_axis',(0.,-1.,0.));
#9682=DIRECTION('ref_axis',(1.,0.,0.));
#9683=DIRECTION('',(-0.707106781186547,0.707106781186548,-8.65956056235493E-17));
#9684=DIRECTION('center_axis',(0.,-1.,0.));
#9685=DIRECTION('ref_axis',(0.,0.,-1.));
#9686=DIRECTION('center_axis',(0.,-1.,0.));
#9687=DIRECTION('ref_axis',(1.,0.,0.));
#9688=DIRECTION('center_axis',(0.,1.,0.));
#9689=DIRECTION('ref_axis',(1.,0.,0.));
#9690=DIRECTION('center_axis',(0.,1.,0.));
#9691=DIRECTION('ref_axis',(1.,0.,0.));
#9692=DIRECTION('',(-0.447213595499958,0.894427190999916,-5.47678698264203E-17));
#9693=DIRECTION('center_axis',(0.,-1.,0.));
#9694=DIRECTION('ref_axis',(1.,0.,0.));
#9695=DIRECTION('',(0.,1.,0.));
#11834=CARTESIAN_POINT('',(0.,0.,0.));
#11835=CARTESIAN_POINT('Origin',(0.115470053837925,-0.5,-0.2));
#11836=CARTESIAN_POINT('',(0.23094010767585,-0.5,0.));
#11837=CARTESIAN_POINT('',(0.115470053837925,-0.5,-0.2));
#11838=CARTESIAN_POINT('',(0.23094010767585,-0.5,0.));
#11839=CARTESIAN_POINT('',(0.115470053837925,-0.8,-0.2));
#11840=CARTESIAN_POINT('',(0.115470053837925,-0.5,-0.2));
#11841=CARTESIAN_POINT('',(0.23094010767585,-0.8,0.));
#11842=CARTESIAN_POINT('',(0.23094010767585,-0.8,0.));
#11843=CARTESIAN_POINT('',(0.23094010767585,-0.5,0.));
#11844=CARTESIAN_POINT('Origin',(-0.115470053837925,-0.5,-0.2));
#11845=CARTESIAN_POINT('',(-0.115470053837925,-0.5,-0.2));
#11846=CARTESIAN_POINT('',(0.115470053837925,-0.5,-0.2));
#11847=CARTESIAN_POINT('',(-0.115470053837925,-0.8,-0.2));
#11848=CARTESIAN_POINT('',(-0.115470053837925,-0.5,-0.2));
#11849=CARTESIAN_POINT('',(0.115470053837925,-0.8,-0.2));
#11850=CARTESIAN_POINT('Origin',(-0.23094010767585,-0.5,-2.77555756156289E-17));
#11851=CARTESIAN_POINT('',(-0.23094010767585,-0.5,-2.82820063659975E-17));
#11852=CARTESIAN_POINT('',(-0.115470053837925,-0.5,-0.2));
#11853=CARTESIAN_POINT('',(-0.23094010767585,-0.8,-2.77555756156289E-17));
#11854=CARTESIAN_POINT('',(-0.23094010767585,-0.5,-2.82820063659975E-17));
#11855=CARTESIAN_POINT('',(-0.115470053837925,-0.8,-0.2));
#11856=CARTESIAN_POINT('Origin',(-0.115470053837925,-0.5,0.2));
#11857=CARTESIAN_POINT('',(-0.115470053837925,-0.5,0.2));
#11858=CARTESIAN_POINT('',(-0.23094010767585,-0.5,-2.82820063659975E-17));
#11859=CARTESIAN_POINT('',(-0.115470053837925,-0.8,0.2));
#11860=CARTESIAN_POINT('',(-0.115470053837925,-0.5,0.2));
#11861=CARTESIAN_POINT('',(-0.23094010767585,-0.8,-2.82820063659975E-17));
#11862=CARTESIAN_POINT('Origin',(0.115470053837925,-0.5,0.2));
#11863=CARTESIAN_POINT('',(0.115470053837925,-0.5,0.2));
#11864=CARTESIAN_POINT('',(-0.115470053837925,-0.5,0.2));
#11865=CARTESIAN_POINT('',(0.115470053837925,-0.8,0.2));
#11866=CARTESIAN_POINT('',(0.115470053837925,-0.5,0.2));
#11867=CARTESIAN_POINT('',(-0.115470053837925,-0.8,0.2));
#11868=CARTESIAN_POINT('Origin',(0.23094010767585,-0.5,0.));
#11869=CARTESIAN_POINT('',(0.115470053837925,-0.5,0.2));
#11870=CARTESIAN_POINT('',(0.115470053837925,-0.8,0.2));
#11871=CARTESIAN_POINT('Origin',(0.,-0.5,0.));
#11872=CARTESIAN_POINT('Origin',(0.,-0.8,0.));
#11873=CARTESIAN_POINT('Origin',(0.,-1.4,0.));
#11874=CARTESIAN_POINT('',(-0.24505,-1.4,3.00099698131059E-17));
#11875=CARTESIAN_POINT('Origin',(0.,-1.4,0.));
#11876=CARTESIAN_POINT('Origin',(0.375,0.5,0.));
#11877=CARTESIAN_POINT('',(-0.375,0.5,-4.59242549680257E-17));
#11878=CARTESIAN_POINT('Origin',(0.,0.5,0.));
#11879=CARTESIAN_POINT('Origin',(0.,0.475,0.));
#11880=CARTESIAN_POINT('',(-0.425,0.45,-5.20474889637625E-17));
#11881=CARTESIAN_POINT('Origin',(0.,0.45,0.));
#11882=CARTESIAN_POINT('',(-0.4,0.475,-4.89858719658941E-17));
#11883=CARTESIAN_POINT('Origin',(0.,0.24,0.));
#11884=CARTESIAN_POINT('',(-0.425,0.0299999999999998,-5.20474889637625E-17));
#11885=CARTESIAN_POINT('Origin',(0.,0.0299999999999998,0.));
#11886=CARTESIAN_POINT('',(-0.425,0.24,-5.20474889637625E-17));
#11887=CARTESIAN_POINT('Origin',(0.,0.0150000000000001,0.));
#11888=CARTESIAN_POINT('',(-0.395,4.85722573273506E-17,-4.83735485663204E-17));
#11889=CARTESIAN_POINT('Origin',(0.,0.,0.));
#11890=CARTESIAN_POINT('',(-0.41,0.0150000000000001,-5.02105187650415E-17));
#11891=CARTESIAN_POINT('Origin',(0.27,0.,0.));
#11892=CARTESIAN_POINT('',(-0.27,0.,-3.30654635769785E-17));
#11893=CARTESIAN_POINT('Origin',(0.,0.,0.));
#11894=CARTESIAN_POINT('Origin',(0.,-0.02,0.));
#11895=CARTESIAN_POINT('',(-0.24505,-0.0498999999999999,3.00099698131059E-17));
#11896=CARTESIAN_POINT('Origin',(0.,-0.0498999999999999,0.));
#11897=CARTESIAN_POINT('',(-0.26,-0.02,-3.18408167778312E-17));
#11898=CARTESIAN_POINT('Origin',(0.,-0.995,0.));
#11899=CARTESIAN_POINT('',(-0.24505,-0.995,-3.00099698131059E-17));
#12753=UNCERTAINTY_MEASURE_WITH_UNIT(LENGTH_MEASURE(0.001),#12805,
'DISTANCE_ACCURACY_VALUE',
'Maximum model space distance between geometric entities at asserted c
onnectivities');
#12768=UNCERTAINTY_MEASURE_WITH_UNIT(LENGTH_MEASURE(0.001),#12805,
'DISTANCE_ACCURACY_VALUE',
'Maximum model space distance between geometric entities at asserted c
onnectivities');
#12789=(
GEOMETRIC_REPRESENTATION_CONTEXT(3)
GLOBAL_UNCERTAINTY_ASSIGNED_CONTEXT((#12753))
GLOBAL_UNIT_ASSIGNED_CONTEXT((#12805,#12807,#12808))
REPRESENTATION_CONTEXT('','3D')
);
#12804=(
GEOMETRIC_REPRESENTATION_CONTEXT(3)
GLOBAL_UNCERTAINTY_ASSIGNED_CONTEXT((#12768))
GLOBAL_UNIT_ASSIGNED_CONTEXT((#12805,#12807,#12808))
REPRESENTATION_CONTEXT('','3D')
);
#12805=(
LENGTH_UNIT()
NAMED_UNIT(*)
SI_UNIT(.CENTI.,.METRE.)
);
#12807=(
NAMED_UNIT(*)
PLANE_ANGLE_UNIT()
SI_UNIT($,.RADIAN.)
);
#12808=(
NAMED_UNIT(*)
SI_UNIT($,.STERADIAN.)
SOLID_ANGLE_UNIT()
);
#12829=SHAPE_DEFINITION_REPRESENTATION(#12864,#13019);
#12864=PRODUCT_DEFINITION_SHAPE('',$,#13055);
#13019=SHAPE_REPRESENTATION('',(#8085),#12789);
#13034=PRODUCT_DEFINITION_CONTEXT('part definition',#13141,'design');
#13055=PRODUCT_DEFINITION('M5x14 Cap Screw','M5x14 Cap Screw',#13090,#13034);
#13090=PRODUCT_DEFINITION_FORMATION('',$,#13163);
#13141=APPLICATION_CONTEXT(
'Core Data for Automotive Mechanical Design Process');
#13142=PRODUCT_CONTEXT('part definition',#13141,'mechanical');
#13163=PRODUCT('M5x14 Cap Screw','M5x14 Cap Screw','M5x14 Cap Screw',(#13142));
#13248=COLOUR_RGB('Black',0.12,0.14,0.17);
#13249=FILL_AREA_STYLE_COLOUR('',#13248);
#13250=FILL_AREA_STYLE('',(#13249));
#13251=SURFACE_STYLE_FILL_AREA(#13250);
#13252=SURFACE_SIDE_STYLE('',(#13251));
#13253=SURFACE_STYLE_USAGE(.BOTH.,#13252);
#13254=PRESENTATION_STYLE_ASSIGNMENT((#13253));
ENDSEC;
END-ISO-10303-21;
